ISO-10303-21;
HEADER;
/* Generated by software containing ST-Developer
 * from STEP Tools, Inc. (www.steptools.com) 
 */

FILE_DESCRIPTION(
/* description */ ('PAT-003'),
/* implementation_level */ '2;1');

FILE_NAME(
/* name */ 'Hex Nut - M8.step',
/* time_stamp */ '2026-10-29T15:45:40-07:00',
/* author */ (''),
/* organization */ (''),
/* preprocessor_version */ 'ST-DEVELOPER v20.2',
/* originating_system */ 'Autodesk Translation Framework v15.17.0.0',
/* authorisation */ '');

FILE_SCHEMA (('AUTOMOTIVE_DESIGN { 1 0 10303 214 3 1 1 }'));
ENDSEC;

DATA;
#10=MECHANICAL_DESIGN_GEOMETRIC_PRESENTATION_REPRESENTATION('',(#157),#5761);
#93=(
BOUNDED_CURVE()
B_SPLINE_CURVE(2,(#5530,#5531,#5532),.UNSPECIFIED.,.F.,.F.)
B_SPLINE_CURVE_WITH_KNOTS((3,3),(0.14973948338295,0.97160236658079),
 .UNSPECIFIED.)
CURVE()
GEOMETRIC_REPRESENTATION_ITEM()
RATIONAL_B_SPLINE_CURVE((1.07140024848292,1.23714644374248,1.07140024848292))
REPRESENTATION_ITEM('')
);
#94=(
BOUNDED_CURVE()
B_SPLINE_CURVE(2,(#5534,#5535,#5536),.UNSPECIFIED.,.F.,.F.)
B_SPLINE_CURVE_WITH_KNOTS((3,3),(0.14973948338295,0.971602366580789),
 .UNSPECIFIED.)
CURVE()
GEOMETRIC_REPRESENTATION_ITEM()
RATIONAL_B_SPLINE_CURVE((1.07140024848292,1.23714644374248,1.07140024848292))
REPRESENTATION_ITEM('')
);
#95=(
BOUNDED_CURVE()
B_SPLINE_CURVE(2,(#5541,#5542,#5543),.UNSPECIFIED.,.F.,.F.)
B_SPLINE_CURVE_WITH_KNOTS((3,3),(0.14973948338295,0.97160236658079),
 .UNSPECIFIED.)
CURVE()
GEOMETRIC_REPRESENTATION_ITEM()
RATIONAL_B_SPLINE_CURVE((1.07140024848292,1.23714644374248,1.07140024848292))
REPRESENTATION_ITEM('')
);
#96=(
BOUNDED_CURVE()
B_SPLINE_CURVE(2,(#5545,#5546,#5547),.UNSPECIFIED.,.F.,.F.)
B_SPLINE_CURVE_WITH_KNOTS((3,3),(0.14973948338295,0.97160236658079),
 .UNSPECIFIED.)
CURVE()
GEOMETRIC_REPRESENTATION_ITEM()
RATIONAL_B_SPLINE_CURVE((1.07140024848292,1.23714644374248,1.07140024848292))
REPRESENTATION_ITEM('')
);
#97=(
BOUNDED_CURVE()
B_SPLINE_CURVE(2,(#5549,#5550,#5551),.UNSPECIFIED.,.F.,.F.)
B_SPLINE_CURVE_WITH_KNOTS((3,3),(0.14973948338295,0.971602366580789),
 .UNSPECIFIED.)
CURVE()
GEOMETRIC_REPRESENTATION_ITEM()
RATIONAL_B_SPLINE_CURVE((1.07140024848292,1.23714644374248,1.07140024848292))
REPRESENTATION_ITEM('')
);
#98=(
BOUNDED_CURVE()
B_SPLINE_CURVE(2,(#5552,#5553,#5554),.UNSPECIFIED.,.F.,.F.)
B_SPLINE_CURVE_WITH_KNOTS((3,3),(0.14973948338295,0.97160236658079),
 .UNSPECIFIED.)
CURVE()
GEOMETRIC_REPRESENTATION_ITEM()
RATIONAL_B_SPLINE_CURVE((1.07140024848292,1.23714644374248,1.07140024848292))
REPRESENTATION_ITEM('')
);
#99=(
BOUNDED_CURVE()
B_SPLINE_CURVE(2,(#5561,#5562,#5563),.UNSPECIFIED.,.F.,.F.)
B_SPLINE_CURVE_WITH_KNOTS((3,3),(0.14973948338295,0.97160236658079),
 .UNSPECIFIED.)
CURVE()
GEOMETRIC_REPRESENTATION_ITEM()
RATIONAL_B_SPLINE_CURVE((1.07140024848292,1.23714644374248,1.07140024848292))
REPRESENTATION_ITEM('')
);
#100=(
BOUNDED_CURVE()
B_SPLINE_CURVE(2,(#5565,#5566,#5567),.UNSPECIFIED.,.F.,.F.)
B_SPLINE_CURVE_WITH_KNOTS((3,3),(0.14973948338295,0.97160236658079),
 .UNSPECIFIED.)
CURVE()
GEOMETRIC_REPRESENTATION_ITEM()
RATIONAL_B_SPLINE_CURVE((1.07140024848292,1.23714644374248,1.07140024848292))
REPRESENTATION_ITEM('')
);
#101=(
BOUNDED_CURVE()
B_SPLINE_CURVE(2,(#5569,#5570,#5571),.UNSPECIFIED.,.F.,.F.)
B_SPLINE_CURVE_WITH_KNOTS((3,3),(0.14973948338295,0.971602366580789),
 .UNSPECIFIED.)
CURVE()
GEOMETRIC_REPRESENTATION_ITEM()
RATIONAL_B_SPLINE_CURVE((1.07140024848292,1.23714644374248,1.07140024848292))
REPRESENTATION_ITEM('')
);
#102=(
BOUNDED_CURVE()
B_SPLINE_CURVE(2,(#5573,#5574,#5575),.UNSPECIFIED.,.F.,.F.)
B_SPLINE_CURVE_WITH_KNOTS((3,3),(0.14973948338295,0.97160236658079),
 .UNSPECIFIED.)
CURVE()
GEOMETRIC_REPRESENTATION_ITEM()
RATIONAL_B_SPLINE_CURVE((1.07140024848292,1.23714644374248,1.07140024848292))
REPRESENTATION_ITEM('')
);
#103=(
BOUNDED_CURVE()
B_SPLINE_CURVE(2,(#5577,#5578,#5579),.UNSPECIFIED.,.F.,.F.)
B_SPLINE_CURVE_WITH_KNOTS((3,3),(0.14973948338295,0.97160236658079),
 .UNSPECIFIED.)
CURVE()
GEOMETRIC_REPRESENTATION_ITEM()
RATIONAL_B_SPLINE_CURVE((1.07140024848292,1.23714644374248,1.07140024848292))
REPRESENTATION_ITEM('')
);
#104=(
BOUNDED_CURVE()
B_SPLINE_CURVE(2,(#5580,#5581,#5582),.UNSPECIFIED.,.F.,.F.)
B_SPLINE_CURVE_WITH_KNOTS((3,3),(0.14973948338295,0.971602366580789),
 .UNSPECIFIED.)
CURVE()
GEOMETRIC_REPRESENTATION_ITEM()
RATIONAL_B_SPLINE_CURVE((1.07140024848292,1.23714644374248,1.07140024848292))
REPRESENTATION_ITEM('')
);
#119=CONICAL_SURFACE('',#3714,0.734027674973257,1.0471975511966);
#120=CONICAL_SURFACE('',#3716,0.734027674973257,1.0471975511966);
#133=SHAPE_REPRESENTATION_RELATIONSHIP('SRR','None',#5828,#145);
#145=ADVANCED_BREP_SHAPE_REPRESENTATION('',(#167),#5759);
#157=STYLED_ITEM('',(#5956),#167);
#167=MANIFOLD_SOLID_BREP('Body1',#3333);
#201=FACE_BOUND('',#724,.T.);
#202=FACE_BOUND('',#726,.T.);
#324=PLANE('',#3718);
#325=PLANE('',#3719);
#326=PLANE('',#3720);
#327=PLANE('',#3724);
#328=PLANE('',#3725);
#329=PLANE('',#3726);
#330=PLANE('',#3727);
#331=PLANE('',#3728);
#495=FACE_OUTER_BOUND('',#714,.T.);
#496=FACE_OUTER_BOUND('',#715,.T.);
#497=FACE_OUTER_BOUND('',#716,.T.);
#498=FACE_OUTER_BOUND('',#717,.T.);
#499=FACE_OUTER_BOUND('',#718,.T.);
#500=FACE_OUTER_BOUND('',#719,.T.);
#501=FACE_OUTER_BOUND('',#720,.T.);
#502=FACE_OUTER_BOUND('',#721,.T.);
#503=FACE_OUTER_BOUND('',#722,.T.);
#504=FACE_OUTER_BOUND('',#723,.T.);
#505=FACE_OUTER_BOUND('',#725,.T.);
#714=EDGE_LOOP('',(#2930,#2931,#2932,#2933,#2934,#2935,#2936,#2937,#2938));
#715=EDGE_LOOP('',(#2939,#2940,#2941,#2942,#2943,#2944,#2945,#2946,#2947));
#716=EDGE_LOOP('',(#2948,#2949,#2950,#2951));
#717=EDGE_LOOP('',(#2952,#2953,#2954,#2955));
#718=EDGE_LOOP('',(#2956,#2957,#2958,#2959));
#719=EDGE_LOOP('',(#2960,#2961,#2962,#2963));
#720=EDGE_LOOP('',(#2964,#2965,#2966,#2967));
#721=EDGE_LOOP('',(#2968,#2969,#2970,#2971));
#722=EDGE_LOOP('',(#2972,#2973,#2974,#2975));
#723=EDGE_LOOP('',(#2976));
#724=EDGE_LOOP('',(#2977));
#725=EDGE_LOOP('',(#2978));
#726=EDGE_LOOP('',(#2979));
#1034=LINE('',#5538,#1356);
#1035=LINE('',#5559,#1357);
#1036=LINE('',#5584,#1358);
#1037=LINE('',#5585,#1359);
#1038=LINE('',#5587,#1360);
#1039=LINE('',#5589,#1361);
#1040=LINE('',#5594,#1362);
#1041=LINE('',#5597,#1363);
#1042=LINE('',#5599,#1364);
#1356=VECTOR('',#4563,0.734027674973257);
#1357=VECTOR('',#4570,0.734027674973257);
#1358=VECTOR('',#4573,1.);
#1359=VECTOR('',#4574,1.);
#1360=VECTOR('',#4577,1.);
#1361=VECTOR('',#4580,1.);
#1362=VECTOR('',#4585,0.4);
#1363=VECTOR('',#4590,1.);
#1364=VECTOR('',#4593,1.);
#1462=CIRCLE('',#3715,0.6175);
#1463=CIRCLE('',#3717,0.6175);
#1464=CIRCLE('',#3722,0.338975);
#1465=CIRCLE('',#3723,0.338975);
#1726=VERTEX_POINT('',#5528);
#1727=VERTEX_POINT('',#5529);
#1728=VERTEX_POINT('',#5533);
#1729=VERTEX_POINT('',#5537);
#1730=VERTEX_POINT('',#5540);
#1731=VERTEX_POINT('',#5544);
#1732=VERTEX_POINT('',#5548);
#1733=VERTEX_POINT('',#5556);
#1734=VERTEX_POINT('',#5558);
#1735=VERTEX_POINT('',#5560);
#1736=VERTEX_POINT('',#5564);
#1737=VERTEX_POINT('',#5568);
#1738=VERTEX_POINT('',#5572);
#1739=VERTEX_POINT('',#5576);
#1740=VERTEX_POINT('',#5591);
#1741=VERTEX_POINT('',#5593);
#2136=EDGE_CURVE('',#1726,#1727,#93,.T.);
#2137=EDGE_CURVE('',#1728,#1726,#94,.T.);
#2138=EDGE_CURVE('',#1728,#1729,#1034,.T.);
#2139=EDGE_CURVE('',#1729,#1729,#1462,.T.);
#2140=EDGE_CURVE('',#1730,#1728,#95,.T.);
#2141=EDGE_CURVE('',#1731,#1730,#96,.T.);
#2142=EDGE_CURVE('',#1732,#1731,#97,.T.);
#2143=EDGE_CURVE('',#1727,#1732,#98,.T.);
#2144=EDGE_CURVE('',#1733,#1733,#1463,.T.);
#2145=EDGE_CURVE('',#1733,#1734,#1035,.T.);
#2146=EDGE_CURVE('',#1735,#1734,#99,.T.);
#2147=EDGE_CURVE('',#1736,#1735,#100,.T.);
#2148=EDGE_CURVE('',#1737,#1736,#101,.T.);
#2149=EDGE_CURVE('',#1738,#1737,#102,.T.);
#2150=EDGE_CURVE('',#1739,#1738,#103,.T.);
#2151=EDGE_CURVE('',#1734,#1739,#104,.T.);
#2152=EDGE_CURVE('',#1730,#1739,#1036,.T.);
#2153=EDGE_CURVE('',#1731,#1738,#1037,.T.);
#2154=EDGE_CURVE('',#1728,#1734,#1038,.T.);
#2155=EDGE_CURVE('',#1726,#1735,#1039,.T.);
#2156=EDGE_CURVE('',#1740,#1740,#1464,.F.);
#2157=EDGE_CURVE('',#1740,#1741,#1040,.T.);
#2158=EDGE_CURVE('',#1741,#1741,#1465,.F.);
#2159=EDGE_CURVE('',#1727,#1736,#1041,.T.);
#2160=EDGE_CURVE('',#1732,#1737,#1042,.T.);
#2930=ORIENTED_EDGE('',*,*,#2136,.F.);
#2931=ORIENTED_EDGE('',*,*,#2137,.F.);
#2932=ORIENTED_EDGE('',*,*,#2138,.T.);
#2933=ORIENTED_EDGE('',*,*,#2139,.F.);
#2934=ORIENTED_EDGE('',*,*,#2138,.F.);
#2935=ORIENTED_EDGE('',*,*,#2140,.F.);
#2936=ORIENTED_EDGE('',*,*,#2141,.F.);
#2937=ORIENTED_EDGE('',*,*,#2142,.F.);
#2938=ORIENTED_EDGE('',*,*,#2143,.F.);
#2939=ORIENTED_EDGE('',*,*,#2144,.F.);
#2940=ORIENTED_EDGE('',*,*,#2145,.T.);
#2941=ORIENTED_EDGE('',*,*,#2146,.F.);
#2942=ORIENTED_EDGE('',*,*,#2147,.F.);
#2943=ORIENTED_EDGE('',*,*,#2148,.F.);
#2944=ORIENTED_EDGE('',*,*,#2149,.F.);
#2945=ORIENTED_EDGE('',*,*,#2150,.F.);
#2946=ORIENTED_EDGE('',*,*,#2151,.F.);
#2947=ORIENTED_EDGE('',*,*,#2145,.F.);
#2948=ORIENTED_EDGE('',*,*,#2141,.T.);
#2949=ORIENTED_EDGE('',*,*,#2152,.T.);
#2950=ORIENTED_EDGE('',*,*,#2150,.T.);
#2951=ORIENTED_EDGE('',*,*,#2153,.F.);
#2952=ORIENTED_EDGE('',*,*,#2140,.T.);
#2953=ORIENTED_EDGE('',*,*,#2154,.T.);
#2954=ORIENTED_EDGE('',*,*,#2151,.T.);
#2955=ORIENTED_EDGE('',*,*,#2152,.F.);
#2956=ORIENTED_EDGE('',*,*,#2137,.T.);
#2957=ORIENTED_EDGE('',*,*,#2155,.T.);
#2958=ORIENTED_EDGE('',*,*,#2146,.T.);
#2959=ORIENTED_EDGE('',*,*,#2154,.F.);
#2960=ORIENTED_EDGE('',*,*,#2156,.F.);
#2961=ORIENTED_EDGE('',*,*,#2157,.T.);
#2962=ORIENTED_EDGE('',*,*,#2158,.T.);
#2963=ORIENTED_EDGE('',*,*,#2157,.F.);
#2964=ORIENTED_EDGE('',*,*,#2136,.T.);
#2965=ORIENTED_EDGE('',*,*,#2159,.T.);
#2966=ORIENTED_EDGE('',*,*,#2147,.T.);
#2967=ORIENTED_EDGE('',*,*,#2155,.F.);
#2968=ORIENTED_EDGE('',*,*,#2142,.T.);
#2969=ORIENTED_EDGE('',*,*,#2153,.T.);
#2970=ORIENTED_EDGE('',*,*,#2149,.T.);
#2971=ORIENTED_EDGE('',*,*,#2160,.F.);
#2972=ORIENTED_EDGE('',*,*,#2143,.T.);
#2973=ORIENTED_EDGE('',*,*,#2160,.T.);
#2974=ORIENTED_EDGE('',*,*,#2148,.T.);
#2975=ORIENTED_EDGE('',*,*,#2159,.F.);
#2976=ORIENTED_EDGE('',*,*,#2144,.T.);
#2977=ORIENTED_EDGE('',*,*,#2156,.T.);
#2978=ORIENTED_EDGE('',*,*,#2139,.T.);
#2979=ORIENTED_EDGE('',*,*,#2158,.F.);
#3120=CYLINDRICAL_SURFACE('',#3721,0.338975);
#3288=ADVANCED_FACE('',(#495),#119,.T.);
#3289=ADVANCED_FACE('',(#496),#120,.T.);
#3290=ADVANCED_FACE('',(#497),#324,.T.);
#3291=ADVANCED_FACE('',(#498),#325,.T.);
#3292=ADVANCED_FACE('',(#499),#326,.T.);
#3293=ADVANCED_FACE('',(#500),#3120,.F.);
#3294=ADVANCED_FACE('',(#501),#327,.T.);
#3295=ADVANCED_FACE('',(#502),#328,.T.);
#3296=ADVANCED_FACE('',(#503),#329,.T.);
#3297=ADVANCED_FACE('',(#504,#201),#330,.T.);
#3298=ADVANCED_FACE('',(#505,#202),#331,.F.);
#3333=CLOSED_SHELL('',(#3288,#3289,#3290,#3291,#3292,#3293,#3294,#3295,
#3296,#3297,#3298));
#3713=AXIS2_PLACEMENT_3D('',#5526,#4559,#4560);
#3714=AXIS2_PLACEMENT_3D('',#5527,#4561,#4562);
#3715=AXIS2_PLACEMENT_3D('',#5539,#4564,#4565);
#3716=AXIS2_PLACEMENT_3D('',#5555,#4566,#4567);
#3717=AXIS2_PLACEMENT_3D('',#5557,#4568,#4569);
#3718=AXIS2_PLACEMENT_3D('',#5583,#4571,#4572);
#3719=AXIS2_PLACEMENT_3D('',#5586,#4575,#4576);
#3720=AXIS2_PLACEMENT_3D('',#5588,#4578,#4579);
#3721=AXIS2_PLACEMENT_3D('',#5590,#4581,#4582);
#3722=AXIS2_PLACEMENT_3D('',#5592,#4583,#4584);
#3723=AXIS2_PLACEMENT_3D('',#5595,#4586,#4587);
#3724=AXIS2_PLACEMENT_3D('',#5596,#4588,#4589);
#3725=AXIS2_PLACEMENT_3D('',#5598,#4591,#4592);
#3726=AXIS2_PLACEMENT_3D('',#5600,#4594,#4595);
#3727=AXIS2_PLACEMENT_3D('',#5601,#4596,#4597);
#3728=AXIS2_PLACEMENT_3D('',#5602,#4598,#4599);
#4559=DIRECTION('axis',(0.,0.,1.));
#4560=DIRECTION('refdir',(1.,0.,0.));
#4561=DIRECTION('center_axis',(0.,1.,0.));
#4562=DIRECTION('ref_axis',(1.,0.,0.));
#4563=DIRECTION('',(0.866025403784439,-0.5,1.06057523872491E-16));
#4564=DIRECTION('center_axis',(0.,-1.,0.));
#4565=DIRECTION('ref_axis',(1.,0.,0.));
#4566=DIRECTION('center_axis',(0.,-1.,0.));
#4567=DIRECTION('ref_axis',(1.,0.,0.));
#4568=DIRECTION('center_axis',(0.,1.,0.));
#4569=DIRECTION('ref_axis',(1.,0.,0.));
#4570=DIRECTION('',(-0.866025403784439,-0.5,-1.06057523872491E-16));
#4571=DIRECTION('center_axis',(1.4792020664489E-16,0.,-1.));
#4572=DIRECTION('ref_axis',(-1.,0.,-1.4792020664489E-16));
#4573=DIRECTION('',(0.,1.,0.));
#4574=DIRECTION('',(0.,1.,0.));
#4575=DIRECTION('center_axis',(-0.866025403784439,0.,-0.5));
#4576=DIRECTION('ref_axis',(-0.5,0.,0.866025403784439));
#4577=DIRECTION('',(0.,1.,0.));
#4578=DIRECTION('center_axis',(-0.866025403784439,0.,0.5));
#4579=DIRECTION('ref_axis',(0.5,0.,0.866025403784439));
#4580=DIRECTION('',(0.,1.,0.));
#4581=DIRECTION('center_axis',(0.,1.,0.));
#4582=DIRECTION('ref_axis',(1.,0.,0.));
#4583=DIRECTION('center_axis',(0.,1.,0.));
#4584=DIRECTION('ref_axis',(1.,0.,0.));
#4585=DIRECTION('',(0.,-1.,0.));
#4586=DIRECTION('center_axis',(0.,1.,0.));
#4587=DIRECTION('ref_axis',(1.,0.,0.));
#4588=DIRECTION('center_axis',(-2.95840413289779E-16,0.,1.));
#4589=DIRECTION('ref_axis',(1.,0.,2.95840413289779E-16));
#4590=DIRECTION('',(0.,1.,0.));
#4591=DIRECTION('center_axis',(0.866025403784439,0.,-0.5));
#4592=DIRECTION('ref_axis',(-0.5,0.,-0.866025403784439));
#4593=DIRECTION('',(0.,1.,0.));
#4594=DIRECTION('center_axis',(0.866025403784439,0.,0.5));
#4595=DIRECTION('ref_axis',(0.5,0.,-0.866025403784439));
#4596=DIRECTION('center_axis',(0.,1.,0.));
#4597=DIRECTION('ref_axis',(1.,0.,0.));
#4598=DIRECTION('center_axis',(0.,1.,0.));
#4599=DIRECTION('ref_axis',(1.,0.,0.));
#5526=CARTESIAN_POINT('',(0.,0.,0.));
#5527=CARTESIAN_POINT('Origin',(0.,0.067277284513851,0.));
#5528=CARTESIAN_POINT('',(-0.375277674973257,0.0768195421087395,0.65));
#5529=CARTESIAN_POINT('',(0.375277674973257,0.0768195421087395,0.65));
#5530=CARTESIAN_POINT('Ctrl Pts',(-0.375277674973257,0.0768195421087395,
0.65));
#5531=CARTESIAN_POINT('Ctrl Pts',(1.66533453693773E-13,-0.0315137912242439,
0.65));
#5532=CARTESIAN_POINT('Ctrl Pts',(0.375277674973257,0.0768195421087394,
0.65));
#5533=CARTESIAN_POINT('',(-0.750555349946514,0.0768195421087394,-9.19165206894919E-17));
#5534=CARTESIAN_POINT('Ctrl Pts',(-0.750555349946514,0.0768195421087394,
-9.19165206894919E-17));
#5535=CARTESIAN_POINT('Ctrl Pts',(-0.562916512459802,-0.0315137912242434,
0.325000000000144));
#5536=CARTESIAN_POINT('Ctrl Pts',(-0.375277674973257,0.0768195421087395,
0.65));
#5537=CARTESIAN_POINT('',(-0.6175,-2.77555756156289E-17,-7.5621939847349E-17));
#5538=CARTESIAN_POINT('',(-0.734027674973257,0.067277284513851,-8.98924642641573E-17));
#5539=CARTESIAN_POINT('Origin',(0.,0.,0.));
#5540=CARTESIAN_POINT('',(-0.375277674973257,0.0768195421087395,-0.65));
#5541=CARTESIAN_POINT('Ctrl Pts',(-0.375277674973257,0.0768195421087395,
-0.65));
#5542=CARTESIAN_POINT('Ctrl Pts',(-0.562916512459968,-0.0315137912242437,
-0.324999999999856));
#5543=CARTESIAN_POINT('Ctrl Pts',(-0.750555349946514,0.0768195421087395,
-9.19165206894919E-17));
#5544=CARTESIAN_POINT('',(0.375277674973257,0.0768195421087395,-0.65));
#5545=CARTESIAN_POINT('Ctrl Pts',(0.375277674973257,0.0768195421087395,
-0.65));
#5546=CARTESIAN_POINT('Ctrl Pts',(-1.66144875635155E-13,-0.0315137912242437,
-0.65));
#5547=CARTESIAN_POINT('Ctrl Pts',(-0.375277674973257,0.0768195421087395,
-0.65));
#5548=CARTESIAN_POINT('',(0.750555349946514,0.0768195421087394,0.));
#5549=CARTESIAN_POINT('Ctrl Pts',(0.750555349946514,0.0768195421087394,
0.));
#5550=CARTESIAN_POINT('Ctrl Pts',(0.562916512459802,-0.0315137912242436,
-0.325000000000144));
#5551=CARTESIAN_POINT('Ctrl Pts',(0.375277674973257,0.0768195421087395,
-0.65));
#5552=CARTESIAN_POINT('Ctrl Pts',(0.375277674973257,0.0768195421087394,
0.65));
#5553=CARTESIAN_POINT('Ctrl Pts',(0.562916512459968,-0.0315137912242439,
0.324999999999856));
#5554=CARTESIAN_POINT('Ctrl Pts',(0.750555349946514,0.0768195421087394,
0.));
#5555=CARTESIAN_POINT('Origin',(0.,0.612722715486149,0.));
#5556=CARTESIAN_POINT('',(-0.6175,0.68,-7.5621939847349E-17));
#5557=CARTESIAN_POINT('Origin',(0.,0.68,0.));
#5558=CARTESIAN_POINT('',(-0.750555349946514,0.603180457891261,-9.19165206894919E-17));
#5559=CARTESIAN_POINT('',(-0.734027674973257,0.612722715486149,-8.98924642641573E-17));
#5560=CARTESIAN_POINT('',(-0.375277674973257,0.603180457891261,0.65));
#5561=CARTESIAN_POINT('Ctrl Pts',(-0.375277674973257,0.603180457891261,
0.65));
#5562=CARTESIAN_POINT('Ctrl Pts',(-0.562916512459968,0.711513791224243,
0.324999999999856));
#5563=CARTESIAN_POINT('Ctrl Pts',(-0.750555349946514,0.603180457891261,
-9.19165206894919E-17));
#5564=CARTESIAN_POINT('',(0.375277674973257,0.603180457891261,0.65));
#5565=CARTESIAN_POINT('Ctrl Pts',(0.375277674973257,0.603180457891261,0.65));
#5566=CARTESIAN_POINT('Ctrl Pts',(-1.66755498298699E-13,0.711513791224244,
0.65));
#5567=CARTESIAN_POINT('Ctrl Pts',(-0.375277674973257,0.603180457891261,
0.65));
#5568=CARTESIAN_POINT('',(0.750555349946514,0.603180457891261,0.));
#5569=CARTESIAN_POINT('Ctrl Pts',(0.750555349946514,0.603180457891261,0.));
#5570=CARTESIAN_POINT('Ctrl Pts',(0.562916512459802,0.711513791224244,0.325000000000144));
#5571=CARTESIAN_POINT('Ctrl Pts',(0.375277674973257,0.603180457891261,0.65));
#5572=CARTESIAN_POINT('',(0.375277674973257,0.603180457891261,-0.65));
#5573=CARTESIAN_POINT('Ctrl Pts',(0.375277674973257,0.603180457891261,-0.65));
#5574=CARTESIAN_POINT('Ctrl Pts',(0.562916512459969,0.711513791224244,-0.324999999999856));
#5575=CARTESIAN_POINT('Ctrl Pts',(0.750555349946514,0.603180457891261,0.));
#5576=CARTESIAN_POINT('',(-0.375277674973257,0.603180457891261,-0.65));
#5577=CARTESIAN_POINT('Ctrl Pts',(-0.375277674973257,0.603180457891261,
-0.65));
#5578=CARTESIAN_POINT('Ctrl Pts',(1.66422431391311E-13,0.711513791224244,
-0.65));
#5579=CARTESIAN_POINT('Ctrl Pts',(0.375277674973257,0.603180457891261,-0.65));
#5580=CARTESIAN_POINT('Ctrl Pts',(-0.750555349946514,0.603180457891261,
-9.19165206894919E-17));
#5581=CARTESIAN_POINT('Ctrl Pts',(-0.562916512459802,0.711513791224244,
-0.325000000000144));
#5582=CARTESIAN_POINT('Ctrl Pts',(-0.375277674973257,0.603180457891261,
-0.65));
#5583=CARTESIAN_POINT('Origin',(0.375277674973257,0.,-0.65));
#5584=CARTESIAN_POINT('',(-0.375277674973257,0.,-0.65));
#5585=CARTESIAN_POINT('',(0.375277674973257,0.,-0.65));
#5586=CARTESIAN_POINT('Origin',(-0.375277674973257,0.,-0.65));
#5587=CARTESIAN_POINT('',(-0.750555349946514,0.,-9.19165206894919E-17));
#5588=CARTESIAN_POINT('Origin',(-0.750555349946514,0.,-9.19165206894919E-17));
#5589=CARTESIAN_POINT('',(-0.375277674973257,0.,0.65));
#5590=CARTESIAN_POINT('Origin',(0.,0.,0.));
#5591=CARTESIAN_POINT('',(-0.338975,0.68,4.15124648740974E-17));
#5592=CARTESIAN_POINT('Origin',(0.,0.68,0.));
#5593=CARTESIAN_POINT('',(-0.338975,0.,4.15124648740974E-17));
#5594=CARTESIAN_POINT('',(-0.338975,0.,4.15124648740974E-17));
#5595=CARTESIAN_POINT('Origin',(0.,0.,0.));
#5596=CARTESIAN_POINT('Origin',(-0.375277674973257,0.,0.65));
#5597=CARTESIAN_POINT('',(0.375277674973257,0.,0.65));
#5598=CARTESIAN_POINT('Origin',(0.750555349946514,0.,0.));
#5599=CARTESIAN_POINT('',(0.750555349946514,0.,0.));
#5600=CARTESIAN_POINT('Origin',(0.375277674973257,0.,0.65));
#5601=CARTESIAN_POINT('Origin',(0.,0.68,-1.11022302462516E-16));
#5602=CARTESIAN_POINT('Origin',(0.,0.,-1.11022302462516E-16));
#5743=UNCERTAINTY_MEASURE_WITH_UNIT(LENGTH_MEASURE(0.001),#5762,
'DISTANCE_ACCURACY_VALUE',
'Maximum model space distance between geometric entities at asserted c
onnectivities');
#5745=UNCERTAINTY_MEASURE_WITH_UNIT(LENGTH_MEASURE(0.001),#5762,
'DISTANCE_ACCURACY_VALUE',
'Maximum model space distance between geometric entities at asserted c
onnectivities');
#5759=(
GEOMETRIC_REPRESENTATION_CONTEXT(3)
GLOBAL_UNCERTAINTY_ASSIGNED_CONTEXT((#5743))
GLOBAL_UNIT_ASSIGNED_CONTEXT((#5762,#5764,#5765))
REPRESENTATION_CONTEXT('','3D')
);
#5761=(
GEOMETRIC_REPRESENTATION_CONTEXT(3)
GLOBAL_UNCERTAINTY_ASSIGNED_CONTEXT((#5745))
GLOBAL_UNIT_ASSIGNED_CONTEXT((#5762,#5764,#5765))
REPRESENTATION_CONTEXT('','3D')
);
#5762=(
LENGTH_UNIT()
NAMED_UNIT(*)
SI_UNIT(.CENTI.,.METRE.)
);
#5764=(
NAMED_UNIT(*)
PLANE_ANGLE_UNIT()
SI_UNIT($,.RADIAN.)
);
#5765=(
NAMED_UNIT(*)
SI_UNIT($,.STERADIAN.)
SOLID_ANGLE_UNIT()
);
#5779=SHAPE_DEFINITION_REPRESENTATION(#5804,#5828);
#5804=PRODUCT_DEFINITION_SHAPE('',$,#5844);
#5828=SHAPE_REPRESENTATION('',(#3713),#5759);
#5830=PRODUCT_DEFINITION_CONTEXT('part definition',#5877,'design');
#5844=PRODUCT_DEFINITION('Hex Nut - M8','Hex Nut - M8',#5859,#5830);
#5859=PRODUCT_DEFINITION_FORMATION('',$,#5892);
#5877=APPLICATION_CONTEXT(
'Core Data for Automotive Mechanical Design Process');
#5878=PRODUCT_CONTEXT('part definition',#5877,'mechanical');
#5892=PRODUCT('Hex Nut - M8','Hex Nut - M8','Hex Nut - M8',(#5878));
#5950=COLOUR_RGB('Black',0.12,0.14,0.17);
#5951=FILL_AREA_STYLE_COLOUR('',#5950);
#5952=FILL_AREA_STYLE('',(#5951));
#5953=SURFACE_STYLE_FILL_AREA(#5952);
#5954=SURFACE_SIDE_STYLE('',(#5953));
#5955=SURFACE_STYLE_USAGE(.BOTH.,#5954);
#5956=PRESENTATION_STYLE_ASSIGNMENT((#5955));
ENDSEC;
END-ISO-10303-21;
